ISO-10303-21;
HEADER;
FILE_DESCRIPTION((''),'2;1');
FILE_NAME('Screw_ISO7045_M3x4.step','2026-10-09T09:51:33-07:00',(''),(''),'','','');
FILE_SCHEMA (('AUTOMOTIVE_DESIGN { 1 0 10303 214 3 1 1 }'));
ENDSEC;
DATA;
#10=MECHANICAL_DESIGN_GEOMETRIC_PRESENTATION_REPRESENTATION('',(#4171),#126571);
#67=(
BOUNDED_CURVE()
B_SPLINE_CURVE(2,(#126461,#126462,#126463),.UNSPECIFIED.,.F.,.F.)
B_SPLINE_CURVE_WITH_KNOTS((3,3),(-0.29451811881086,-0.129072001599117),
 .UNSPECIFIED.)
CURVE()
GEOMETRIC_REPRESENTATION_ITEM()
RATIONAL_B_SPLINE_CURVE((1.01263937277422,1.02259966004803,1.01738098005117))
REPRESENTATION_ITEM('')
) ;
#68=(
BOUNDED_CURVE()
B_SPLINE_CURVE(2,(#126470,#126471,#126472),.UNSPECIFIED.,.F.,.F.)
B_SPLINE_CURVE_WITH_KNOTS((3,3),(-0.242836044574457,-0.0773899273627136),
 .UNSPECIFIED.)
CURVE()
GEOMETRIC_REPRESENTATION_ITEM()
RATIONAL_B_SPLINE_CURVE((1.01738098005117,1.02259966004803,1.01263937277422))
REPRESENTATION_ITEM('')
) ;
#69=(
BOUNDED_CURVE()
B_SPLINE_CURVE(2,(#126477,#126478,#126479),.UNSPECIFIED.,.F.,.F.)
B_SPLINE_CURVE_WITH_KNOTS((3,3),(-0.242836044574458,-0.0773899273627143),
 .UNSPECIFIED.)
CURVE()
GEOMETRIC_REPRESENTATION_ITEM()
RATIONAL_B_SPLINE_CURVE((1.01738098005117,1.02259966004802,1.01263937277422))
REPRESENTATION_ITEM('')
) ;
#70=(
BOUNDED_CURVE()
B_SPLINE_CURVE(2,(#126482,#126483,#126484),.UNSPECIFIED.,.F.,.F.)
B_SPLINE_CURVE_WITH_KNOTS((3,3),(-0.294518118810858,-0.129072001599116),
 .UNSPECIFIED.)
CURVE()
GEOMETRIC_REPRESENTATION_ITEM()
RATIONAL_B_SPLINE_CURVE((1.01263937277421,1.02259966004801,1.01738098005116))
REPRESENTATION_ITEM('')
) ;
#71=(
BOUNDED_CURVE()
B_SPLINE_CURVE(2,(#126513,#126514,#126515),.UNSPECIFIED.,.F.,.F.)
B_SPLINE_CURVE_WITH_KNOTS((3,3),(-0.294518118811012,-0.129072001599294),
 .UNSPECIFIED.)
CURVE()
GEOMETRIC_REPRESENTATION_ITEM()
RATIONAL_B_SPLINE_CURVE((1.01263937277418,1.02259966004795,1.01738098005112))
REPRESENTATION_ITEM('')
) ;
#72=(
BOUNDED_CURVE()
B_SPLINE_CURVE(2,(#126520,#126521,#126522),.UNSPECIFIED.,.F.,.F.)
B_SPLINE_CURVE_WITH_KNOTS((3,3),(-0.242836044574467,-0.0773899273627484),
 .UNSPECIFIED.)
CURVE()
GEOMETRIC_REPRESENTATION_ITEM()
RATIONAL_B_SPLINE_CURVE((1.01738098005112,1.02259966004794,1.01263937277417))
REPRESENTATION_ITEM('')
) ;
#73=(
BOUNDED_CURVE()
B_SPLINE_CURVE(2,(#126531,#126532,#126533),.UNSPECIFIED.,.F.,.F.)
B_SPLINE_CURVE_WITH_KNOTS((3,3),(-0.242836044574484,-0.0773899273627661),
 .UNSPECIFIED.)
CURVE()
GEOMETRIC_REPRESENTATION_ITEM()
RATIONAL_B_SPLINE_CURVE((1.01738098005103,1.02259966004783,1.01263937277412))
REPRESENTATION_ITEM('')
) ;
#74=(
BOUNDED_CURVE()
B_SPLINE_CURVE(2,(#126535,#126536,#126537),.UNSPECIFIED.,.F.,.F.)
B_SPLINE_CURVE_WITH_KNOTS((3,3),(-0.294518118811009,-0.129072001599291),
 .UNSPECIFIED.)
CURVE()
GEOMETRIC_REPRESENTATION_ITEM()
RATIONAL_B_SPLINE_CURVE((1.01263937277417,1.02259966004793,1.01738098005111))
REPRESENTATION_ITEM('')
) ;
#474=SHAPE_REPRESENTATION_RELATIONSHIP('SRR','None',#126604,#480) ;
#480=ADVANCED_BREP_SHAPE_REPRESENTATION('',(#4181),#126570) ;
#4171=STYLED_ITEM('',(#126645),#4181) ;
#4181=MANIFOLD_SOLID_BREP('Body1',#67695) ;
#4839=SPHERICAL_SURFACE('',#76795,5.) ;
#4985=ELLIPSE('',#76782,1.10195897608265,0.486831694836699) ;
#4986=ELLIPSE('',#76817,1.10195897609098,0.486831694838641) ;
#4987=ELLIPSE('',#76819,1.10195897609068,0.486831694838579) ;
#4988=ELLIPSE('',#76831,1.1019589760921,0.486831694838885) ;
#5063=FACE_BOUND('',#24688,.T.) ;
#5064=FACE_BOUND('',#24709,.T.) ;
#5925=PLANE('',#76812) ;
#5926=PLANE('',#76813) ;
#5927=PLANE('',#76814) ;
#5928=PLANE('',#76815) ;
#5929=PLANE('',#76816) ;
#5930=PLANE('',#76818) ;
#5931=PLANE('',#76820) ;
#5932=PLANE('',#76821) ;
#5933=PLANE('',#76822) ;
#5934=PLANE('',#76823) ;
#5935=PLANE('',#76824) ;
#5936=PLANE('',#76825) ;
#5937=PLANE('',#76826) ;
#5938=PLANE('',#76827) ;
#5939=PLANE('',#76828) ;
#5940=PLANE('',#76829) ;
#5941=PLANE('',#76830) ;
#5942=PLANE('',#76832) ;
#5943=PLANE('',#76833) ;
#5944=PLANE('',#76834) ;
#5945=PLANE('',#76835) ;
#5946=PLANE('',#76836) ;
#7894=CYLINDRICAL_SURFACE('',#76791,2.8) ;
#7895=CYLINDRICAL_SURFACE('',#76793,1.5) ;
#11985=LINE('',#126371,#16101) ;
#11986=LINE('',#126421,#16102) ;
#11987=LINE('',#126425,#16103) ;
#11988=LINE('',#126465,#16104) ;
#11989=LINE('',#126466,#16105) ;
#11990=LINE('',#126469,#16106) ;
#11991=LINE('',#126473,#16107) ;
#11992=LINE('',#126476,#16108) ;
#11993=LINE('',#126480,#16109) ;
#11994=LINE('',#126486,#16110) ;
#11995=LINE('',#126487,#16111) ;
#11996=LINE('',#126490,#16112) ;
#11997=LINE('',#126491,#16113) ;
#11998=LINE('',#126494,#16114) ;
#11999=LINE('',#126495,#16115) ;
#12000=LINE('',#126498,#16116) ;
#12001=LINE('',#126499,#16117) ;
#12002=LINE('',#126504,#16118) ;
#12003=LINE('',#126505,#16119) ;
#12004=LINE('',#126508,#16120) ;
#12005=LINE('',#126509,#16121) ;
#12006=LINE('',#126517,#16122) ;
#12007=LINE('',#126518,#16123) ;
#12008=LINE('',#126523,#16124) ;
#12009=LINE('',#126525,#16125) ;
#12010=LINE('',#126528,#16126) ;
#12011=LINE('',#126529,#16127) ;
#16101=VECTOR('',#98943,3077.68353717531) ;
#16102=VECTOR('',#99000,2.8) ;
#16103=VECTOR('',#99005,1.5) ;
#16104=VECTOR('',#99044,1000.) ;
#16105=VECTOR('',#99045,1000.) ;
#16106=VECTOR('',#99048,1000.) ;
#16107=VECTOR('',#99049,1000.) ;
#16108=VECTOR('',#99052,1000.) ;
#16109=VECTOR('',#99053,1000.) ;
#16110=VECTOR('',#99056,1000.) ;
#16111=VECTOR('',#99057,1000.) ;
#16112=VECTOR('',#99062,1000.) ;
#16113=VECTOR('',#99063,1000.) ;
#16114=VECTOR('',#99068,1000.) ;
#16115=VECTOR('',#99069,1000.) ;
#16116=VECTOR('',#99072,1000.) ;
#16117=VECTOR('',#99073,1000.) ;
#16118=VECTOR('',#99080,1000.) ;
#16119=VECTOR('',#99081,1000.) ;
#16120=VECTOR('',#99084,1000.) ;
#16121=VECTOR('',#99085,1000.) ;
#16122=VECTOR('',#99092,1000.) ;
#16123=VECTOR('',#99093,1000.) ;
#16124=VECTOR('',#99096,1000.) ;
#16125=VECTOR('',#99099,1000.) ;
#16126=VECTOR('',#99104,1000.) ;
#16127=VECTOR('',#99105,1000.) ;
#16150=CONICAL_SURFACE('',#76763,3077.68353717531,1.25663706143592) ;
#16151=CONICAL_SURFACE('',#76781,0.556,0.0698131700797659) ;
#16152=CONICAL_SURFACE('',#76837,0.556,0.0698131700797659) ;
#16153=CONICAL_SURFACE('',#76838,0.556,0.0698131700797659) ;
#16154=CONICAL_SURFACE('',#76839,0.556,0.0698131700797659) ;
#16155=CONICAL_SURFACE('',#76840,0.556,0.0698131700797659) ;
#16156=CONICAL_SURFACE('',#76841,0.556,0.0698131700797659) ;
#16157=CONICAL_SURFACE('',#76842,0.556,0.0698131700797659) ;
#16158=CONICAL_SURFACE('',#76843,0.556,0.0698131700797659) ;
#20365=FACE_OUTER_BOUND('',#24681,.T.) ;
#20366=FACE_OUTER_BOUND('',#24682,.T.) ;
#20367=FACE_OUTER_BOUND('',#24683,.T.) ;
#20368=FACE_OUTER_BOUND('',#24684,.T.) ;
#20369=FACE_OUTER_BOUND('',#24685,.T.) ;
#20370=FACE_OUTER_BOUND('',#24686,.T.) ;
#20371=FACE_OUTER_BOUND('',#24687,.T.) ;
#20372=FACE_OUTER_BOUND('',#24689,.T.) ;
#20373=FACE_OUTER_BOUND('',#24690,.T.) ;
#20374=FACE_OUTER_BOUND('',#24691,.T.) ;
#20375=FACE_OUTER_BOUND('',#24692,.T.) ;
#20376=FACE_OUTER_BOUND('',#24693,.T.) ;
#20377=FACE_OUTER_BOUND('',#24694,.T.) ;
#20378=FACE_OUTER_BOUND('',#24695,.T.) ;
#20379=FACE_OUTER_BOUND('',#24696,.T.) ;
#20380=FACE_OUTER_BOUND('',#24697,.T.) ;
#20381=FACE_OUTER_BOUND('',#24698,.T.) ;
#20382=FACE_OUTER_BOUND('',#24699,.T.) ;
#20383=FACE_OUTER_BOUND('',#24700,.T.) ;
#20384=FACE_OUTER_BOUND('',#24701,.T.) ;
#20385=FACE_OUTER_BOUND('',#24702,.T.) ;
#20386=FACE_OUTER_BOUND('',#24703,.T.) ;
#20387=FACE_OUTER_BOUND('',#24704,.T.) ;
#20388=FACE_OUTER_BOUND('',#24705,.T.) ;
#20389=FACE_OUTER_BOUND('',#24706,.T.) ;
#20390=FACE_OUTER_BOUND('',#24707,.T.) ;
#20391=FACE_OUTER_BOUND('',#24708,.T.) ;
#20392=FACE_OUTER_BOUND('',#24710,.T.) ;
#20393=FACE_OUTER_BOUND('',#24711,.T.) ;
#20394=FACE_OUTER_BOUND('',#24712,.T.) ;
#20395=FACE_OUTER_BOUND('',#24713,.T.) ;
#20396=FACE_OUTER_BOUND('',#24714,.T.) ;
#20397=FACE_OUTER_BOUND('',#24715,.T.) ;
#20398=FACE_OUTER_BOUND('',#24716,.T.) ;
#20399=FACE_OUTER_BOUND('',#24717,.T.) ;
#20400=FACE_OUTER_BOUND('',#24718,.T.) ;
#24681=EDGE_LOOP('',(#62654,#62655,#62656,#62657,#62658,#62659,#62660,#62661,
#62662,#62663,#62664,#62665,#62666,#62667,#62668,#62669,#62670,#62671,#62672)) ;
#24682=EDGE_LOOP('',(#62673,#62674)) ;
#24683=EDGE_LOOP('',(#62675,#62676,#62677,#62678)) ;
#24684=EDGE_LOOP('',(#62679,#62680,#62681,#62682)) ;
#24685=EDGE_LOOP('',(#62683,#62684,#62685,#62686)) ;
#24686=EDGE_LOOP('',(#62687,#62688,#62689,#62690)) ;
#24687=EDGE_LOOP('',(#62691)) ;
#24688=EDGE_LOOP('',(#62692,#62693,#62694,#62695,#62696,#62697,#62698,#62699,
#62700,#62701,#62702,#62703,#62704,#62705,#62706,#62707)) ;
#24689=EDGE_LOOP('',(#62708,#62709,#62710,#62711)) ;
#24690=EDGE_LOOP('',(#62712,#62713,#62714,#62715)) ;
#24691=EDGE_LOOP('',(#62716,#62717,#62718,#62719)) ;
#24692=EDGE_LOOP('',(#62720,#62721,#62722,#62723)) ;
#24693=EDGE_LOOP('',(#62724,#62725,#62726,#62727,#62728,#62729)) ;
#24694=EDGE_LOOP('',(#62730,#62731,#62732,#62733,#62734,#62735)) ;
#24695=EDGE_LOOP('',(#62736,#62737,#62738)) ;
#24696=EDGE_LOOP('',(#62739,#62740,#62741)) ;
#24697=EDGE_LOOP('',(#62742,#62743,#62744)) ;
#24698=EDGE_LOOP('',(#62745,#62746,#62747)) ;
#24699=EDGE_LOOP('',(#62748,#62749,#62750)) ;
#24700=EDGE_LOOP('',(#62751,#62752,#62753)) ;
#24701=EDGE_LOOP('',(#62754,#62755,#62756)) ;
#24702=EDGE_LOOP('',(#62757,#62758,#62759,#62760)) ;
#24703=EDGE_LOOP('',(#62761,#62762,#62763,#62764)) ;
#24704=EDGE_LOOP('',(#62765,#62766,#62767,#62768,#62769,#62770)) ;
#24705=EDGE_LOOP('',(#62771,#62772,#62773,#62774,#62775,#62776)) ;
#24706=EDGE_LOOP('',(#62777,#62778,#62779,#62780)) ;
#24707=EDGE_LOOP('',(#62781,#62782,#62783,#62784)) ;
#24708=EDGE_LOOP('',(#62785)) ;
#24709=EDGE_LOOP('',(#62786)) ;
#24710=EDGE_LOOP('',(#62787)) ;
#24711=EDGE_LOOP('',(#62788,#62789,#62790)) ;
#24712=EDGE_LOOP('',(#62791,#62792)) ;
#24713=EDGE_LOOP('',(#62793,#62794)) ;
#24714=EDGE_LOOP('',(#62795,#62796,#62797,#62798)) ;
#24715=EDGE_LOOP('',(#62799,#62800,#62801)) ;
#24716=EDGE_LOOP('',(#62802,#62803,#62804,#62805)) ;
#24717=EDGE_LOOP('',(#62806,#62807,#62808,#62809)) ;
#24718=EDGE_LOOP('',(#62810,#62811,#62812,#62813)) ;
#29453=CIRCLE('',#76764,0.556) ;
#29454=CIRCLE('',#76765,0.556) ;
#29455=CIRCLE('',#76766,0.556) ;
#29456=CIRCLE('',#76767,0.556) ;
#29457=CIRCLE('',#76768,0.556) ;
#29458=CIRCLE('',#76769,0.556) ;
#29459=CIRCLE('',#76770,0.556) ;
#29460=CIRCLE('',#76771,0.556) ;
#29461=CIRCLE('',#76772,0.556) ;
#29462=CIRCLE('',#76773,0.556) ;
#29463=CIRCLE('',#76774,0.556) ;
#29464=CIRCLE('',#76775,0.556) ;
#29465=CIRCLE('',#76776,0.556) ;
#29466=CIRCLE('',#76777,0.556) ;
#29467=CIRCLE('',#76778,0.556) ;
#29468=CIRCLE('',#76779,0.556) ;
#29469=CIRCLE('',#76780,0.556) ;
#29470=CIRCLE('',#76784,1.6) ;
#29471=CIRCLE('',#76785,0.1) ;
#29472=CIRCLE('',#76786,1.5) ;
#29473=CIRCLE('',#76788,2.67441860465116) ;
#29474=CIRCLE('',#76789,0.27) ;
#29475=CIRCLE('',#76790,2.8) ;
#29476=CIRCLE('',#76792,2.8) ;
#29477=CIRCLE('',#76794,1.5) ;
#29478=CIRCLE('',#76796,4.90340272700175) ;
#29479=CIRCLE('',#76797,4.98629120689917) ;
#29480=CIRCLE('',#76798,0.675169614150692) ;
#29481=CIRCLE('',#76799,4.98629120689917) ;
#29482=CIRCLE('',#76800,4.90340272700175) ;
#29483=CIRCLE('',#76801,4.98629120689917) ;
#29484=CIRCLE('',#76802,0.675169614150692) ;
#29485=CIRCLE('',#76803,4.98629120689917) ;
#29486=CIRCLE('',#76804,4.90340272700175) ;
#29487=CIRCLE('',#76805,4.98629120689917) ;
#29488=CIRCLE('',#76806,0.675169614150692) ;
#29489=CIRCLE('',#76807,4.98629120689917) ;
#29490=CIRCLE('',#76808,4.90340272700175) ;
#29491=CIRCLE('',#76809,4.98629120689917) ;
#29492=CIRCLE('',#76810,0.675169614150692) ;
#29493=CIRCLE('',#76811,4.98629120689917) ;
#34644=VERTEX_POINT('',#126369) ;
#34645=VERTEX_POINT('',#126370) ;
#34646=VERTEX_POINT('',#126372) ;
#34647=VERTEX_POINT('',#126374) ;
#34648=VERTEX_POINT('',#126376) ;
#34649=VERTEX_POINT('',#126378) ;
#34650=VERTEX_POINT('',#126380) ;
#34651=VERTEX_POINT('',#126382) ;
#34652=VERTEX_POINT('',#126384) ;
#34653=VERTEX_POINT('',#126386) ;
#34654=VERTEX_POINT('',#126388) ;
#34655=VERTEX_POINT('',#126390) ;
#34656=VERTEX_POINT('',#126392) ;
#34657=VERTEX_POINT('',#126394) ;
#34658=VERTEX_POINT('',#126396) ;
#34659=VERTEX_POINT('',#126398) ;
#34660=VERTEX_POINT('',#126400) ;
#34661=VERTEX_POINT('',#126402) ;
#34662=VERTEX_POINT('',#126408) ;
#34663=VERTEX_POINT('',#126410) ;
#34664=VERTEX_POINT('',#126414) ;
#34665=VERTEX_POINT('',#126416) ;
#34666=VERTEX_POINT('',#126420) ;
#34667=VERTEX_POINT('',#126424) ;
#34668=VERTEX_POINT('',#126428) ;
#34669=VERTEX_POINT('',#126429) ;
#34670=VERTEX_POINT('',#126431) ;
#34671=VERTEX_POINT('',#126433) ;
#34672=VERTEX_POINT('',#126435) ;
#34673=VERTEX_POINT('',#126437) ;
#34674=VERTEX_POINT('',#126439) ;
#34675=VERTEX_POINT('',#126441) ;
#34676=VERTEX_POINT('',#126443) ;
#34677=VERTEX_POINT('',#126445) ;
#34678=VERTEX_POINT('',#126447) ;
#34679=VERTEX_POINT('',#126449) ;
#34680=VERTEX_POINT('',#126451) ;
#34681=VERTEX_POINT('',#126453) ;
#34682=VERTEX_POINT('',#126455) ;
#34683=VERTEX_POINT('',#126457) ;
#34684=VERTEX_POINT('',#126464) ;
#34685=VERTEX_POINT('',#126468) ;
#34686=VERTEX_POINT('',#126475) ;
#34687=VERTEX_POINT('',#126485) ;
#34688=VERTEX_POINT('',#126497) ;
#34689=VERTEX_POINT('',#126503) ;
#34690=VERTEX_POINT('',#126507) ;
#34691=VERTEX_POINT('',#126516) ;
#43986=EDGE_CURVE('',#34644,#34645,#11985,.T.) ;
#43987=EDGE_CURVE('',#34645,#34646,#29453,.T.) ;
#43988=EDGE_CURVE('',#34646,#34647,#29454,.T.) ;
#43989=EDGE_CURVE('',#34647,#34648,#29455,.T.) ;
#43990=EDGE_CURVE('',#34648,#34649,#29456,.T.) ;
#43991=EDGE_CURVE('',#34649,#34650,#29457,.T.) ;
#43992=EDGE_CURVE('',#34650,#34651,#29458,.T.) ;
#43993=EDGE_CURVE('',#34651,#34652,#29459,.T.) ;
#43994=EDGE_CURVE('',#34652,#34653,#29460,.T.) ;
#43995=EDGE_CURVE('',#34653,#34654,#29461,.T.) ;
#43996=EDGE_CURVE('',#34654,#34655,#29462,.T.) ;
#43997=EDGE_CURVE('',#34655,#34656,#29463,.T.) ;
#43998=EDGE_CURVE('',#34656,#34657,#29464,.T.) ;
#43999=EDGE_CURVE('',#34657,#34658,#29465,.T.) ;
#44000=EDGE_CURVE('',#34658,#34659,#29466,.T.) ;
#44001=EDGE_CURVE('',#34659,#34660,#29467,.T.) ;
#44002=EDGE_CURVE('',#34660,#34661,#29468,.T.) ;
#44003=EDGE_CURVE('',#34661,#34645,#29469,.T.) ;
#44004=EDGE_CURVE('',#34653,#34654,#4985,.T.) ;
#44005=EDGE_CURVE('',#34662,#34662,#29470,.T.) ;
#44006=EDGE_CURVE('',#34662,#34663,#29471,.T.) ;
#44007=EDGE_CURVE('',#34663,#34663,#29472,.T.) ;
#44008=EDGE_CURVE('',#34664,#34664,#29473,.T.) ;
#44009=EDGE_CURVE('',#34664,#34665,#29474,.T.) ;
#44010=EDGE_CURVE('',#34665,#34665,#29475,.T.) ;
#44011=EDGE_CURVE('',#34665,#34666,#11986,.T.) ;
#44012=EDGE_CURVE('',#34666,#34666,#29476,.T.) ;
#44013=EDGE_CURVE('',#34663,#34667,#11987,.T.) ;
#44014=EDGE_CURVE('',#34667,#34667,#29477,.T.) ;
#44015=EDGE_CURVE('',#34668,#34669,#29478,.T.) ;
#44016=EDGE_CURVE('',#34670,#34669,#29479,.T.) ;
#44017=EDGE_CURVE('',#34671,#34670,#29480,.T.) ;
#44018=EDGE_CURVE('',#34672,#34671,#29481,.T.) ;
#44019=EDGE_CURVE('',#34672,#34673,#29482,.T.) ;
#44020=EDGE_CURVE('',#34674,#34673,#29483,.T.) ;
#44021=EDGE_CURVE('',#34675,#34674,#29484,.T.) ;
#44022=EDGE_CURVE('',#34676,#34675,#29485,.T.) ;
#44023=EDGE_CURVE('',#34676,#34677,#29486,.T.) ;
#44024=EDGE_CURVE('',#34678,#34677,#29487,.T.) ;
#44025=EDGE_CURVE('',#34679,#34678,#29488,.T.) ;
#44026=EDGE_CURVE('',#34680,#34679,#29489,.T.) ;
#44027=EDGE_CURVE('',#34680,#34681,#29490,.T.) ;
#44028=EDGE_CURVE('',#34682,#34681,#29491,.T.) ;
#44029=EDGE_CURVE('',#34683,#34682,#29492,.T.) ;
#44030=EDGE_CURVE('',#34668,#34683,#29493,.T.) ;
#44031=EDGE_CURVE('',#34683,#34659,#67,.T.) ;
#44032=EDGE_CURVE('',#34659,#34684,#11988,.T.) ;
#44033=EDGE_CURVE('',#34668,#34684,#11989,.T.) ;
#44034=EDGE_CURVE('',#34685,#34648,#11990,.T.) ;
#44035=EDGE_CURVE('',#34648,#34678,#68,.T.) ;
#44036=EDGE_CURVE('',#34677,#34685,#11991,.T.) ;
#44037=EDGE_CURVE('',#34686,#34656,#11992,.T.) ;
#44038=EDGE_CURVE('',#34656,#34670,#69,.T.) ;
#44039=EDGE_CURVE('',#34669,#34686,#11993,.T.) ;
#44040=EDGE_CURVE('',#34675,#34651,#70,.T.) ;
#44041=EDGE_CURVE('',#34651,#34687,#11994,.T.) ;
#44042=EDGE_CURVE('',#34676,#34687,#11995,.T.) ;
#44043=EDGE_CURVE('',#34657,#34658,#4986,.T.) ;
#44044=EDGE_CURVE('',#34686,#34657,#11996,.T.) ;
#44045=EDGE_CURVE('',#34658,#34684,#11997,.T.) ;
#44046=EDGE_CURVE('',#34649,#34650,#4987,.T.) ;
#44047=EDGE_CURVE('',#34685,#34649,#11998,.T.) ;
#44048=EDGE_CURVE('',#34650,#34687,#11999,.T.) ;
#44049=EDGE_CURVE('',#34688,#34653,#12000,.T.) ;
#44050=EDGE_CURVE('',#34688,#34652,#12001,.T.) ;
#44051=EDGE_CURVE('',#34647,#34689,#12002,.T.) ;
#44052=EDGE_CURVE('',#34646,#34689,#12003,.T.) ;
#44053=EDGE_CURVE('',#34690,#34661,#12004,.T.) ;
#44054=EDGE_CURVE('',#34690,#34660,#12005,.T.) ;
#44055=EDGE_CURVE('',#34671,#34655,#71,.T.) ;
#44056=EDGE_CURVE('',#34655,#34691,#12006,.T.) ;
#44057=EDGE_CURVE('',#34672,#34691,#12007,.T.) ;
#44058=EDGE_CURVE('',#34652,#34674,#72,.T.) ;
#44059=EDGE_CURVE('',#34673,#34688,#12008,.T.) ;
#44060=EDGE_CURVE('',#34654,#34691,#12009,.T.) ;
#44061=EDGE_CURVE('',#34661,#34646,#4988,.T.) ;
#44062=EDGE_CURVE('',#34681,#34690,#12010,.T.) ;
#44063=EDGE_CURVE('',#34680,#34689,#12011,.T.) ;
#44064=EDGE_CURVE('',#34660,#34682,#73,.T.) ;
#44065=EDGE_CURVE('',#34679,#34647,#74,.T.) ;
#62654=ORIENTED_EDGE('',*,*,#43986,.T.) ;
#62655=ORIENTED_EDGE('',*,*,#43987,.T.) ;
#62656=ORIENTED_EDGE('',*,*,#43988,.T.) ;
#62657=ORIENTED_EDGE('',*,*,#43989,.T.) ;
#62658=ORIENTED_EDGE('',*,*,#43990,.T.) ;
#62659=ORIENTED_EDGE('',*,*,#43991,.T.) ;
#62660=ORIENTED_EDGE('',*,*,#43992,.T.) ;
#62661=ORIENTED_EDGE('',*,*,#43993,.T.) ;
#62662=ORIENTED_EDGE('',*,*,#43994,.T.) ;
#62663=ORIENTED_EDGE('',*,*,#43995,.T.) ;
#62664=ORIENTED_EDGE('',*,*,#43996,.T.) ;
#62665=ORIENTED_EDGE('',*,*,#43997,.T.) ;
#62666=ORIENTED_EDGE('',*,*,#43998,.T.) ;
#62667=ORIENTED_EDGE('',*,*,#43999,.T.) ;
#62668=ORIENTED_EDGE('',*,*,#44000,.T.) ;
#62669=ORIENTED_EDGE('',*,*,#44001,.T.) ;
#62670=ORIENTED_EDGE('',*,*,#44002,.T.) ;
#62671=ORIENTED_EDGE('',*,*,#44003,.T.) ;
#62672=ORIENTED_EDGE('',*,*,#43986,.F.) ;
#62673=ORIENTED_EDGE('',*,*,#43995,.F.) ;
#62674=ORIENTED_EDGE('',*,*,#44004,.T.) ;
#62675=ORIENTED_EDGE('',*,*,#44005,.F.) ;
#62676=ORIENTED_EDGE('',*,*,#44006,.T.) ;
#62677=ORIENTED_EDGE('',*,*,#44007,.F.) ;
#62678=ORIENTED_EDGE('',*,*,#44006,.F.) ;
#62679=ORIENTED_EDGE('',*,*,#44008,.F.) ;
#62680=ORIENTED_EDGE('',*,*,#44009,.T.) ;
#62681=ORIENTED_EDGE('',*,*,#44010,.T.) ;
#62682=ORIENTED_EDGE('',*,*,#44009,.F.) ;
#62683=ORIENTED_EDGE('',*,*,#44010,.F.) ;
#62684=ORIENTED_EDGE('',*,*,#44011,.T.) ;
#62685=ORIENTED_EDGE('',*,*,#44012,.T.) ;
#62686=ORIENTED_EDGE('',*,*,#44011,.F.) ;
#62687=ORIENTED_EDGE('',*,*,#44007,.T.) ;
#62688=ORIENTED_EDGE('',*,*,#44013,.T.) ;
#62689=ORIENTED_EDGE('',*,*,#44014,.T.) ;
#62690=ORIENTED_EDGE('',*,*,#44013,.F.) ;
#62691=ORIENTED_EDGE('',*,*,#44008,.T.) ;
#62692=ORIENTED_EDGE('',*,*,#44015,.T.) ;
#62693=ORIENTED_EDGE('',*,*,#44016,.F.) ;
#62694=ORIENTED_EDGE('',*,*,#44017,.F.) ;
#62695=ORIENTED_EDGE('',*,*,#44018,.F.) ;
#62696=ORIENTED_EDGE('',*,*,#44019,.T.) ;
#62697=ORIENTED_EDGE('',*,*,#44020,.F.) ;
#62698=ORIENTED_EDGE('',*,*,#44021,.F.) ;
#62699=ORIENTED_EDGE('',*,*,#44022,.F.) ;
#62700=ORIENTED_EDGE('',*,*,#44023,.T.) ;
#62701=ORIENTED_EDGE('',*,*,#44024,.F.) ;
#62702=ORIENTED_EDGE('',*,*,#44025,.F.) ;
#62703=ORIENTED_EDGE('',*,*,#44026,.F.) ;
#62704=ORIENTED_EDGE('',*,*,#44027,.T.) ;
#62705=ORIENTED_EDGE('',*,*,#44028,.F.) ;
#62706=ORIENTED_EDGE('',*,*,#44029,.F.) ;
#62707=ORIENTED_EDGE('',*,*,#44030,.F.) ;
#62708=ORIENTED_EDGE('',*,*,#44030,.T.) ;
#62709=ORIENTED_EDGE('',*,*,#44031,.T.) ;
#62710=ORIENTED_EDGE('',*,*,#44032,.T.) ;
#62711=ORIENTED_EDGE('',*,*,#44033,.F.) ;
#62712=ORIENTED_EDGE('',*,*,#44034,.T.) ;
#62713=ORIENTED_EDGE('',*,*,#44035,.T.) ;
#62714=ORIENTED_EDGE('',*,*,#44024,.T.) ;
#62715=ORIENTED_EDGE('',*,*,#44036,.T.) ;
#62716=ORIENTED_EDGE('',*,*,#44037,.T.) ;
#62717=ORIENTED_EDGE('',*,*,#44038,.T.) ;
#62718=ORIENTED_EDGE('',*,*,#44016,.T.) ;
#62719=ORIENTED_EDGE('',*,*,#44039,.T.) ;
#62720=ORIENTED_EDGE('',*,*,#44022,.T.) ;
#62721=ORIENTED_EDGE('',*,*,#44040,.T.) ;
#62722=ORIENTED_EDGE('',*,*,#44041,.T.) ;
#62723=ORIENTED_EDGE('',*,*,#44042,.F.) ;
#62724=ORIENTED_EDGE('',*,*,#44043,.F.) ;
#62725=ORIENTED_EDGE('',*,*,#44044,.F.) ;
#62726=ORIENTED_EDGE('',*,*,#44039,.F.) ;
#62727=ORIENTED_EDGE('',*,*,#44015,.F.) ;
#62728=ORIENTED_EDGE('',*,*,#44033,.T.) ;
#62729=ORIENTED_EDGE('',*,*,#44045,.F.) ;
#62730=ORIENTED_EDGE('',*,*,#44046,.F.) ;
#62731=ORIENTED_EDGE('',*,*,#44047,.F.) ;
#62732=ORIENTED_EDGE('',*,*,#44036,.F.) ;
#62733=ORIENTED_EDGE('',*,*,#44023,.F.) ;
#62734=ORIENTED_EDGE('',*,*,#44042,.T.) ;
#62735=ORIENTED_EDGE('',*,*,#44048,.F.) ;
#62736=ORIENTED_EDGE('',*,*,#44049,.T.) ;
#62737=ORIENTED_EDGE('',*,*,#43994,.F.) ;
#62738=ORIENTED_EDGE('',*,*,#44050,.F.) ;
#62739=ORIENTED_EDGE('',*,*,#44041,.F.) ;
#62740=ORIENTED_EDGE('',*,*,#43992,.F.) ;
#62741=ORIENTED_EDGE('',*,*,#44048,.T.) ;
#62742=ORIENTED_EDGE('',*,*,#44047,.T.) ;
#62743=ORIENTED_EDGE('',*,*,#43990,.F.) ;
#62744=ORIENTED_EDGE('',*,*,#44034,.F.) ;
#62745=ORIENTED_EDGE('',*,*,#44051,.F.) ;
#62746=ORIENTED_EDGE('',*,*,#43988,.F.) ;
#62747=ORIENTED_EDGE('',*,*,#44052,.T.) ;
#62748=ORIENTED_EDGE('',*,*,#44053,.T.) ;
#62749=ORIENTED_EDGE('',*,*,#44002,.F.) ;
#62750=ORIENTED_EDGE('',*,*,#44054,.F.) ;
#62751=ORIENTED_EDGE('',*,*,#44032,.F.) ;
#62752=ORIENTED_EDGE('',*,*,#44000,.F.) ;
#62753=ORIENTED_EDGE('',*,*,#44045,.T.) ;
#62754=ORIENTED_EDGE('',*,*,#44044,.T.) ;
#62755=ORIENTED_EDGE('',*,*,#43998,.F.) ;
#62756=ORIENTED_EDGE('',*,*,#44037,.F.) ;
#62757=ORIENTED_EDGE('',*,*,#44018,.T.) ;
#62758=ORIENTED_EDGE('',*,*,#44055,.T.) ;
#62759=ORIENTED_EDGE('',*,*,#44056,.T.) ;
#62760=ORIENTED_EDGE('',*,*,#44057,.F.) ;
#62761=ORIENTED_EDGE('',*,*,#44050,.T.) ;
#62762=ORIENTED_EDGE('',*,*,#44058,.T.) ;
#62763=ORIENTED_EDGE('',*,*,#44020,.T.) ;
#62764=ORIENTED_EDGE('',*,*,#44059,.T.) ;
#62765=ORIENTED_EDGE('',*,*,#44004,.F.) ;
#62766=ORIENTED_EDGE('',*,*,#44049,.F.) ;
#62767=ORIENTED_EDGE('',*,*,#44059,.F.) ;
#62768=ORIENTED_EDGE('',*,*,#44019,.F.) ;
#62769=ORIENTED_EDGE('',*,*,#44057,.T.) ;
#62770=ORIENTED_EDGE('',*,*,#44060,.F.) ;
#62771=ORIENTED_EDGE('',*,*,#44061,.F.) ;
#62772=ORIENTED_EDGE('',*,*,#44053,.F.) ;
#62773=ORIENTED_EDGE('',*,*,#44062,.F.) ;
#62774=ORIENTED_EDGE('',*,*,#44027,.F.) ;
#62775=ORIENTED_EDGE('',*,*,#44063,.T.) ;
#62776=ORIENTED_EDGE('',*,*,#44052,.F.) ;
#62777=ORIENTED_EDGE('',*,*,#44054,.T.) ;
#62778=ORIENTED_EDGE('',*,*,#44064,.T.) ;
#62779=ORIENTED_EDGE('',*,*,#44028,.T.) ;
#62780=ORIENTED_EDGE('',*,*,#44062,.T.) ;
#62781=ORIENTED_EDGE('',*,*,#44026,.T.) ;
#62782=ORIENTED_EDGE('',*,*,#44065,.T.) ;
#62783=ORIENTED_EDGE('',*,*,#44051,.T.) ;
#62784=ORIENTED_EDGE('',*,*,#44063,.F.) ;
#62785=ORIENTED_EDGE('',*,*,#44012,.F.) ;
#62786=ORIENTED_EDGE('',*,*,#44005,.T.) ;
#62787=ORIENTED_EDGE('',*,*,#44014,.F.) ;
#62788=ORIENTED_EDGE('',*,*,#44056,.F.) ;
#62789=ORIENTED_EDGE('',*,*,#43996,.F.) ;
#62790=ORIENTED_EDGE('',*,*,#44060,.T.) ;
#62791=ORIENTED_EDGE('',*,*,#44043,.T.) ;
#62792=ORIENTED_EDGE('',*,*,#43999,.F.) ;
#62793=ORIENTED_EDGE('',*,*,#44046,.T.) ;
#62794=ORIENTED_EDGE('',*,*,#43991,.F.) ;
#62795=ORIENTED_EDGE('',*,*,#43997,.F.) ;
#62796=ORIENTED_EDGE('',*,*,#44055,.F.) ;
#62797=ORIENTED_EDGE('',*,*,#44017,.T.) ;
#62798=ORIENTED_EDGE('',*,*,#44038,.F.) ;
#62799=ORIENTED_EDGE('',*,*,#44061,.T.) ;
#62800=ORIENTED_EDGE('',*,*,#43987,.F.) ;
#62801=ORIENTED_EDGE('',*,*,#44003,.F.) ;
#62802=ORIENTED_EDGE('',*,*,#44021,.T.) ;
#62803=ORIENTED_EDGE('',*,*,#44058,.F.) ;
#62804=ORIENTED_EDGE('',*,*,#43993,.F.) ;
#62805=ORIENTED_EDGE('',*,*,#44040,.F.) ;
#62806=ORIENTED_EDGE('',*,*,#44029,.T.) ;
#62807=ORIENTED_EDGE('',*,*,#44064,.F.) ;
#62808=ORIENTED_EDGE('',*,*,#44001,.F.) ;
#62809=ORIENTED_EDGE('',*,*,#44031,.F.) ;
#62810=ORIENTED_EDGE('',*,*,#43989,.F.) ;
#62811=ORIENTED_EDGE('',*,*,#44065,.F.) ;
#62812=ORIENTED_EDGE('',*,*,#44025,.T.) ;
#62813=ORIENTED_EDGE('',*,*,#44035,.F.) ;
#63442=TOROIDAL_SURFACE('',#76783,1.6,0.1) ;
#63443=TOROIDAL_SURFACE('',#76787,2.53,0.27) ;
#67650=ADVANCED_FACE('',(#20365),#16150,.F.) ;
#67651=ADVANCED_FACE('',(#20366),#16151,.F.) ;
#67652=ADVANCED_FACE('',(#20367),#63442,.F.) ;
#67653=ADVANCED_FACE('',(#20368),#63443,.T.) ;
#67654=ADVANCED_FACE('',(#20369),#7894,.T.) ;
#67655=ADVANCED_FACE('',(#20370),#7895,.T.) ;
#67656=ADVANCED_FACE('',(#20371,#5063),#4839,.T.) ;
#67657=ADVANCED_FACE('',(#20372),#5925,.T.) ;
#67658=ADVANCED_FACE('',(#20373),#5926,.T.) ;
#67659=ADVANCED_FACE('',(#20374),#5927,.T.) ;
#67660=ADVANCED_FACE('',(#20375),#5928,.T.) ;
#67661=ADVANCED_FACE('',(#20376),#5929,.F.) ;
#67662=ADVANCED_FACE('',(#20377),#5930,.F.) ;
#67663=ADVANCED_FACE('',(#20378),#5931,.T.) ;
#67664=ADVANCED_FACE('',(#20379),#5932,.T.) ;
#67665=ADVANCED_FACE('',(#20380),#5933,.T.) ;
#67666=ADVANCED_FACE('',(#20381),#5934,.T.) ;
#67667=ADVANCED_FACE('',(#20382),#5935,.T.) ;
#67668=ADVANCED_FACE('',(#20383),#5936,.T.) ;
#67669=ADVANCED_FACE('',(#20384),#5937,.T.) ;
#67670=ADVANCED_FACE('',(#20385),#5938,.T.) ;
#67671=ADVANCED_FACE('',(#20386),#5939,.T.) ;
#67672=ADVANCED_FACE('',(#20387),#5940,.F.) ;
#67673=ADVANCED_FACE('',(#20388),#5941,.F.) ;
#67674=ADVANCED_FACE('',(#20389),#5942,.T.) ;
#67675=ADVANCED_FACE('',(#20390),#5943,.T.) ;
#67676=ADVANCED_FACE('',(#20391,#5064),#5944,.F.) ;
#67677=ADVANCED_FACE('',(#20392),#5945,.T.) ;
#67678=ADVANCED_FACE('',(#20393),#5946,.T.) ;
#67679=ADVANCED_FACE('',(#20394),#16152,.F.) ;
#67680=ADVANCED_FACE('',(#20395),#16153,.F.) ;
#67681=ADVANCED_FACE('',(#20396),#16154,.F.) ;
#67682=ADVANCED_FACE('',(#20397),#16155,.F.) ;
#67683=ADVANCED_FACE('',(#20398),#16156,.F.) ;
#67684=ADVANCED_FACE('',(#20399),#16157,.F.) ;
#67685=ADVANCED_FACE('',(#20400),#16158,.F.) ;
#67695=CLOSED_SHELL('',(#67650,#67651,#67652,#67653,#67654,#67655,#67656,
#67657,#67658,#67659,#67660,#67661,#67662,#67663,#67664,#67665,#67666,#67667,
#67668,#67669,#67670,#67671,#67672,#67673,#67674,#67675,#67676,#67677,#67678,
#67679,#67680,#67681,#67682,#67683,#67684,#67685)) ;
#76762=AXIS2_PLACEMENT_3D('',#126367,#98939,#98940) ;
#76763=AXIS2_PLACEMENT_3D('',#126368,#98941,#98942) ;
#76764=AXIS2_PLACEMENT_3D('',#126373,#98944,#98945) ;
#76765=AXIS2_PLACEMENT_3D('',#126375,#98946,#98947) ;
#76766=AXIS2_PLACEMENT_3D('',#126377,#98948,#98949) ;
#76767=AXIS2_PLACEMENT_3D('',#126379,#98950,#98951) ;
#76768=AXIS2_PLACEMENT_3D('',#126381,#98952,#98953) ;
#76769=AXIS2_PLACEMENT_3D('',#126383,#98954,#98955) ;
#76770=AXIS2_PLACEMENT_3D('',#126385,#98956,#98957) ;
#76771=AXIS2_PLACEMENT_3D('',#126387,#98958,#98959) ;
#76772=AXIS2_PLACEMENT_3D('',#126389,#98960,#98961) ;
#76773=AXIS2_PLACEMENT_3D('',#126391,#98962,#98963) ;
#76774=AXIS2_PLACEMENT_3D('',#126393,#98964,#98965) ;
#76775=AXIS2_PLACEMENT_3D('',#126395,#98966,#98967) ;
#76776=AXIS2_PLACEMENT_3D('',#126397,#98968,#98969) ;
#76777=AXIS2_PLACEMENT_3D('',#126399,#98970,#98971) ;
#76778=AXIS2_PLACEMENT_3D('',#126401,#98972,#98973) ;
#76779=AXIS2_PLACEMENT_3D('',#126403,#98974,#98975) ;
#76780=AXIS2_PLACEMENT_3D('',#126404,#98976,#98977) ;
#76781=AXIS2_PLACEMENT_3D('',#126405,#98978,#98979) ;
#76782=AXIS2_PLACEMENT_3D('',#126406,#98980,#98981) ;
#76783=AXIS2_PLACEMENT_3D('',#126407,#98982,#98983) ;
#76784=AXIS2_PLACEMENT_3D('',#126409,#98984,#98985) ;
#76785=AXIS2_PLACEMENT_3D('',#126411,#98986,#98987) ;
#76786=AXIS2_PLACEMENT_3D('',#126412,#98988,#98989) ;
#76787=AXIS2_PLACEMENT_3D('',#126413,#98990,#98991) ;
#76788=AXIS2_PLACEMENT_3D('',#126415,#98992,#98993) ;
#76789=AXIS2_PLACEMENT_3D('',#126417,#98994,#98995) ;
#76790=AXIS2_PLACEMENT_3D('',#126418,#98996,#98997) ;
#76791=AXIS2_PLACEMENT_3D('',#126419,#98998,#98999) ;
#76792=AXIS2_PLACEMENT_3D('',#126422,#99001,#99002) ;
#76793=AXIS2_PLACEMENT_3D('',#126423,#99003,#99004) ;
#76794=AXIS2_PLACEMENT_3D('',#126426,#99006,#99007) ;
#76795=AXIS2_PLACEMENT_3D('',#126427,#99008,#99009) ;
#76796=AXIS2_PLACEMENT_3D('',#126430,#99010,#99011) ;
#76797=AXIS2_PLACEMENT_3D('',#126432,#99012,#99013) ;
#76798=AXIS2_PLACEMENT_3D('',#126434,#99014,#99015) ;
#76799=AXIS2_PLACEMENT_3D('',#126436,#99016,#99017) ;
#76800=AXIS2_PLACEMENT_3D('',#126438,#99018,#99019) ;
#76801=AXIS2_PLACEMENT_3D('',#126440,#99020,#99021) ;
#76802=AXIS2_PLACEMENT_3D('',#126442,#99022,#99023) ;
#76803=AXIS2_PLACEMENT_3D('',#126444,#99024,#99025) ;
#76804=AXIS2_PLACEMENT_3D('',#126446,#99026,#99027) ;
#76805=AXIS2_PLACEMENT_3D('',#126448,#99028,#99029) ;
#76806=AXIS2_PLACEMENT_3D('',#126450,#99030,#99031) ;
#76807=AXIS2_PLACEMENT_3D('',#126452,#99032,#99033) ;
#76808=AXIS2_PLACEMENT_3D('',#126454,#99034,#99035) ;
#76809=AXIS2_PLACEMENT_3D('',#126456,#99036,#99037) ;
#76810=AXIS2_PLACEMENT_3D('',#126458,#99038,#99039) ;
#76811=AXIS2_PLACEMENT_3D('',#126459,#99040,#99041) ;
#76812=AXIS2_PLACEMENT_3D('',#126460,#99042,#99043) ;
#76813=AXIS2_PLACEMENT_3D('',#126467,#99046,#99047) ;
#76814=AXIS2_PLACEMENT_3D('',#126474,#99050,#99051) ;
#76815=AXIS2_PLACEMENT_3D('',#126481,#99054,#99055) ;
#76816=AXIS2_PLACEMENT_3D('',#126488,#99058,#99059) ;
#76817=AXIS2_PLACEMENT_3D('',#126489,#99060,#99061) ;
#76818=AXIS2_PLACEMENT_3D('',#126492,#99064,#99065) ;
#76819=AXIS2_PLACEMENT_3D('',#126493,#99066,#99067) ;
#76820=AXIS2_PLACEMENT_3D('',#126496,#99070,#99071) ;
#76821=AXIS2_PLACEMENT_3D('',#126500,#99074,#99075) ;
#76822=AXIS2_PLACEMENT_3D('',#126501,#99076,#99077) ;
#76823=AXIS2_PLACEMENT_3D('',#126502,#99078,#99079) ;
#76824=AXIS2_PLACEMENT_3D('',#126506,#99082,#99083) ;
#76825=AXIS2_PLACEMENT_3D('',#126510,#99086,#99087) ;
#76826=AXIS2_PLACEMENT_3D('',#126511,#99088,#99089) ;
#76827=AXIS2_PLACEMENT_3D('',#126512,#99090,#99091) ;
#76828=AXIS2_PLACEMENT_3D('',#126519,#99094,#99095) ;
#76829=AXIS2_PLACEMENT_3D('',#126524,#99097,#99098) ;
#76830=AXIS2_PLACEMENT_3D('',#126526,#99100,#99101) ;
#76831=AXIS2_PLACEMENT_3D('',#126527,#99102,#99103) ;
#76832=AXIS2_PLACEMENT_3D('',#126530,#99106,#99107) ;
#76833=AXIS2_PLACEMENT_3D('',#126534,#99108,#99109) ;
#76834=AXIS2_PLACEMENT_3D('',#126538,#99110,#99111) ;
#76835=AXIS2_PLACEMENT_3D('',#126539,#99112,#99113) ;
#76836=AXIS2_PLACEMENT_3D('',#126540,#99114,#99115) ;
#76837=AXIS2_PLACEMENT_3D('',#126541,#99116,#99117) ;
#76838=AXIS2_PLACEMENT_3D('',#126542,#99118,#99119) ;
#76839=AXIS2_PLACEMENT_3D('',#126543,#99120,#99121) ;
#76840=AXIS2_PLACEMENT_3D('',#126544,#99122,#99123) ;
#76841=AXIS2_PLACEMENT_3D('',#126545,#99124,#99125) ;
#76842=AXIS2_PLACEMENT_3D('',#126546,#99126,#99127) ;
#76843=AXIS2_PLACEMENT_3D('',#126547,#99128,#99129) ;
#98939=DIRECTION('axis',(0.,0.,1.)) ;
#98940=DIRECTION('refdir',(1.,0.,0.)) ;
#98941=DIRECTION('center_axis',(-1.,0.,0.)) ;
#98942=DIRECTION('ref_axis',(0.,0.,1.)) ;
#98943=DIRECTION('',(-0.309016994374945,-1.16470831848909E-16,-0.951056516295154)) ;
#98944=DIRECTION('center_axis',(-1.,0.,0.)) ;
#98945=DIRECTION('ref_axis',(0.,0.,1.)) ;
#98946=DIRECTION('center_axis',(-1.,0.,0.)) ;
#98947=DIRECTION('ref_axis',(0.,0.,1.)) ;
#98948=DIRECTION('center_axis',(-1.,0.,0.)) ;
#98949=DIRECTION('ref_axis',(0.,0.,1.)) ;
#98950=DIRECTION('center_axis',(-1.,0.,0.)) ;
#98951=DIRECTION('ref_axis',(0.,0.,1.)) ;
#98952=DIRECTION('center_axis',(-1.,0.,0.)) ;
#98953=DIRECTION('ref_axis',(0.,0.,1.)) ;
#98954=DIRECTION('center_axis',(-1.,0.,0.)) ;
#98955=DIRECTION('ref_axis',(0.,0.,1.)) ;
#98956=DIRECTION('center_axis',(-1.,0.,0.)) ;
#98957=DIRECTION('ref_axis',(0.,0.,1.)) ;
#98958=DIRECTION('center_axis',(-1.,0.,0.)) ;
#98959=DIRECTION('ref_axis',(0.,0.,1.)) ;
#98960=DIRECTION('center_axis',(-1.,0.,0.)) ;
#98961=DIRECTION('ref_axis',(0.,0.,1.)) ;
#98962=DIRECTION('center_axis',(-1.,0.,0.)) ;
#98963=DIRECTION('ref_axis',(0.,0.,1.)) ;
#98964=DIRECTION('center_axis',(-1.,0.,0.)) ;
#98965=DIRECTION('ref_axis',(0.,0.,1.)) ;
#98966=DIRECTION('center_axis',(-1.,0.,0.)) ;
#98967=DIRECTION('ref_axis',(0.,0.,1.)) ;
#98968=DIRECTION('center_axis',(-1.,0.,0.)) ;
#98969=DIRECTION('ref_axis',(0.,0.,1.)) ;
#98970=DIRECTION('center_axis',(-1.,0.,0.)) ;
#98971=DIRECTION('ref_axis',(0.,0.,1.)) ;
#98972=DIRECTION('center_axis',(-1.,0.,0.)) ;
#98973=DIRECTION('ref_axis',(0.,0.,1.)) ;
#98974=DIRECTION('center_axis',(-1.,0.,0.)) ;
#98975=DIRECTION('ref_axis',(0.,0.,1.)) ;
#98976=DIRECTION('center_axis',(-1.,0.,0.)) ;
#98977=DIRECTION('ref_axis',(0.,0.,1.)) ;
#98978=DIRECTION('center_axis',(-1.,0.,0.)) ;
#98979=DIRECTION('ref_axis',(0.,0.,1.)) ;
#98980=DIRECTION('center_axis',(-0.446197753347441,5.43259321731477E-15,
-0.89493439139844)) ;
#98981=DIRECTION('ref_axis',(0.89493439139844,8.82040419595591E-13,-0.446197753347441)) ;
#98982=DIRECTION('center_axis',(-1.,0.,0.)) ;
#98983=DIRECTION('ref_axis',(0.,0.,1.)) ;
#98984=DIRECTION('center_axis',(-1.,0.,0.)) ;
#98985=DIRECTION('ref_axis',(0.,0.,1.)) ;
#98986=DIRECTION('center_axis',(0.,1.,-1.22464679914735E-16)) ;
#98987=DIRECTION('ref_axis',(0.,-1.22464679914735E-16,-1.)) ;
#98988=DIRECTION('center_axis',(1.,0.,0.)) ;
#98989=DIRECTION('ref_axis',(0.,0.,1.)) ;
#98990=DIRECTION('center_axis',(-1.,0.,0.)) ;
#98991=DIRECTION('ref_axis',(0.,0.,1.)) ;
#98992=DIRECTION('center_axis',(-1.,0.,0.)) ;
#98993=DIRECTION('ref_axis',(0.,0.,1.)) ;
#98994=DIRECTION('center_axis',(0.,-1.,1.22464679914735E-16)) ;
#98995=DIRECTION('ref_axis',(0.,-1.22464679914735E-16,-1.)) ;
#98996=DIRECTION('center_axis',(-1.,0.,0.)) ;
#98997=DIRECTION('ref_axis',(0.,0.,1.)) ;
#98998=DIRECTION('center_axis',(-1.,0.,0.)) ;
#98999=DIRECTION('ref_axis',(0.,0.,1.)) ;
#99000=DIRECTION('',(1.,0.,0.)) ;
#99001=DIRECTION('center_axis',(-1.,0.,0.)) ;
#99002=DIRECTION('ref_axis',(0.,0.,1.)) ;
#99003=DIRECTION('center_axis',(-1.,0.,0.)) ;
#99004=DIRECTION('ref_axis',(0.,0.,1.)) ;
#99005=DIRECTION('',(1.,0.,0.)) ;
#99006=DIRECTION('center_axis',(-1.,0.,0.)) ;
#99007=DIRECTION('ref_axis',(0.,0.,1.)) ;
#99008=DIRECTION('center_axis',(0.,1.83697019872103E-16,-1.)) ;
#99009=DIRECTION('ref_axis',(0.,1.,1.22464679914735E-16)) ;
#99010=DIRECTION('center_axis',(0.446197753347436,0.894934391398443,0.)) ;
#99011=DIRECTION('ref_axis',(-0.894934391398443,0.446197753347436,0.)) ;
#99012=DIRECTION('center_axis',(7.80261272178311E-17,1.54157131018989E-16,
-1.)) ;
#99013=DIRECTION('ref_axis',(-1.52269221131066E-34,1.,1.54157131018989E-16)) ;
#99014=DIRECTION('center_axis',(-1.,0.,0.)) ;
#99015=DIRECTION('ref_axis',(0.,0.,-1.)) ;
#99016=DIRECTION('center_axis',(0.,-1.,-3.49148133884313E-15)) ;
#99017=DIRECTION('ref_axis',(0.,3.49148133884313E-15,-1.)) ;
#99018=DIRECTION('center_axis',(0.446197753347436,-3.1246467270566E-15,
0.894934391398443)) ;
#99019=DIRECTION('ref_axis',(0.894934391398443,-2.08468151695124E-30,-0.446197753347436)) ;
#99020=DIRECTION('center_axis',(7.80261272178311E-17,1.,3.64563846986212E-15)) ;
#99021=DIRECTION('ref_axis',(-2.78985116612342E-34,-3.64563846986212E-15,
1.)) ;
#99022=DIRECTION('center_axis',(-1.,0.,0.)) ;
#99023=DIRECTION('ref_axis',(0.,0.,-1.)) ;
#99024=DIRECTION('center_axis',(7.80261272178311E-17,1.54157131018989E-16,
-1.)) ;
#99025=DIRECTION('ref_axis',(-1.52269221131066E-34,1.,1.54157131018989E-16)) ;
#99026=DIRECTION('center_axis',(0.446197753347436,-0.894934391398443,0.)) ;
#99027=DIRECTION('ref_axis',(0.894934391398443,0.446197753347436,0.)) ;
#99028=DIRECTION('center_axis',(0.,0.,1.)) ;
#99029=DIRECTION('ref_axis',(1.,0.,0.)) ;
#99030=DIRECTION('center_axis',(-1.,0.,0.)) ;
#99031=DIRECTION('ref_axis',(0.,0.,-1.)) ;
#99032=DIRECTION('center_axis',(7.80261272178311E-17,1.,3.64563846986212E-15)) ;
#99033=DIRECTION('ref_axis',(-2.78985116612342E-34,-3.64563846986212E-15,
1.)) ;
#99034=DIRECTION('center_axis',(0.446197753347436,3.1246467270566E-15,-0.894934391398443)) ;
#99035=DIRECTION('ref_axis',(-0.894934391398443,4.22434834092767E-32,-0.446197753347436)) ;
#99036=DIRECTION('center_axis',(0.,-1.,-3.49148133884313E-15)) ;
#99037=DIRECTION('ref_axis',(0.,3.49148133884313E-15,-1.)) ;
#99038=DIRECTION('center_axis',(-1.,0.,0.)) ;
#99039=DIRECTION('ref_axis',(0.,-4.44089209850063E-15,-1.)) ;
#99040=DIRECTION('center_axis',(0.,0.,1.)) ;
#99041=DIRECTION('ref_axis',(1.,0.,0.)) ;
#99042=DIRECTION('center_axis',(0.,0.,1.)) ;
#99043=DIRECTION('ref_axis',(1.,0.,0.)) ;
#99044=DIRECTION('',(0.,1.,0.)) ;
#99045=DIRECTION('',(0.894934391398443,-0.446197753347436,0.)) ;
#99046=DIRECTION('center_axis',(0.,0.,1.)) ;
#99047=DIRECTION('ref_axis',(1.,0.,0.)) ;
#99048=DIRECTION('',(0.,1.,0.)) ;
#99049=DIRECTION('',(0.894934391398442,0.446197753347436,-2.77225660396053E-17)) ;
#99050=DIRECTION('center_axis',(7.8026127217831E-17,1.54157131018989E-16,
-1.)) ;
#99051=DIRECTION('ref_axis',(0.,1.,1.54157131018989E-16)) ;
#99052=DIRECTION('',(0.,-1.,-1.54157131018989E-16)) ;
#99053=DIRECTION('',(0.894934391398442,-0.446197753347436,5.54451320792105E-17)) ;
#99054=DIRECTION('center_axis',(7.8026127217831E-17,1.54157131018989E-16,
-1.)) ;
#99055=DIRECTION('ref_axis',(0.,1.,1.54157131018989E-16)) ;
#99056=DIRECTION('',(0.,-1.,-1.54157131018989E-16)) ;
#99057=DIRECTION('',(0.894934391398443,0.446197753347436,1.38612830198026E-16)) ;
#99058=DIRECTION('center_axis',(0.446197753347436,0.894934391398443,0.)) ;
#99059=DIRECTION('ref_axis',(-0.894934391398443,0.446197753347436,0.)) ;
#99060=DIRECTION('center_axis',(-0.446197753347433,-0.894934391398444,0.)) ;
#99061=DIRECTION('ref_axis',(0.894934391398444,-0.446197753347433,-4.12152110262257E-18)) ;
#99062=DIRECTION('',(0.,0.,-1.)) ;
#99063=DIRECTION('',(0.,0.,-1.)) ;
#99064=DIRECTION('center_axis',(0.446197753347436,-0.894934391398443,0.)) ;
#99065=DIRECTION('ref_axis',(0.894934391398443,0.446197753347436,0.)) ;
#99066=DIRECTION('center_axis',(-0.446197753347435,0.894934391398443,1.76637751103157E-16)) ;
#99067=DIRECTION('ref_axis',(0.894934391398443,0.446197753347435,4.30154570777946E-16)) ;
#99068=DIRECTION('',(0.,-2.93027614185272E-16,1.)) ;
#99069=DIRECTION('',(0.,-2.93027614185272E-16,1.)) ;
#99070=DIRECTION('center_axis',(-1.,0.,0.)) ;
#99071=DIRECTION('ref_axis',(0.,0.,1.)) ;
#99072=DIRECTION('',(0.,1.,3.49148133884313E-15)) ;
#99073=DIRECTION('',(0.,3.64563846986212E-15,-1.)) ;
#99074=DIRECTION('center_axis',(-1.,0.,0.)) ;
#99075=DIRECTION('ref_axis',(0.,0.,1.)) ;
#99076=DIRECTION('center_axis',(-1.,0.,0.)) ;
#99077=DIRECTION('ref_axis',(0.,0.,1.)) ;
#99078=DIRECTION('center_axis',(-1.,0.,0.)) ;
#99079=DIRECTION('ref_axis',(0.,0.,1.)) ;
#99080=DIRECTION('',(0.,3.64563846986212E-15,-1.)) ;
#99081=DIRECTION('',(0.,-1.,-3.78450895302841E-15)) ;
#99082=DIRECTION('center_axis',(-1.,0.,0.)) ;
#99083=DIRECTION('ref_axis',(0.,0.,1.)) ;
#99084=DIRECTION('',(0.,-1.,-3.78450895302841E-15)) ;
#99085=DIRECTION('',(0.,-3.49148133884313E-15,1.)) ;
#99086=DIRECTION('center_axis',(-1.,0.,0.)) ;
#99087=DIRECTION('ref_axis',(0.,0.,1.)) ;
#99088=DIRECTION('center_axis',(-1.,0.,0.)) ;
#99089=DIRECTION('ref_axis',(0.,0.,1.)) ;
#99090=DIRECTION('center_axis',(0.,-1.,-3.49148133884313E-15)) ;
#99091=DIRECTION('ref_axis',(1.,0.,0.)) ;
#99092=DIRECTION('',(0.,-3.49148133884313E-15,1.)) ;
#99093=DIRECTION('',(0.894934391398443,1.5578911292463E-15,-0.446197753347436)) ;
#99094=DIRECTION('center_axis',(7.8026127217831E-17,1.,3.64563846986212E-15)) ;
#99095=DIRECTION('ref_axis',(-3.38151074872755E-48,-3.64563846986212E-15,
1.)) ;
#99096=DIRECTION('',(0.894934391398442,1.50244599716709E-15,-0.446197753347436)) ;
#99097=DIRECTION('center_axis',(0.446197753347436,-3.1246467270566E-15,
0.894934391398443)) ;
#99098=DIRECTION('ref_axis',(-0.894934391398443,-1.5578911292463E-15,0.446197753347436)) ;
#99099=DIRECTION('',(0.,1.,3.49148133884313E-15)) ;
#99100=DIRECTION('center_axis',(0.446197753347436,3.1246467270566E-15,-0.894934391398443)) ;
#99101=DIRECTION('ref_axis',(0.894934391398443,-1.5578911292463E-15,0.446197753347436)) ;
#99102=DIRECTION('center_axis',(-0.446197753347437,-3.00284176875363E-15,
0.894934391398442)) ;
#99103=DIRECTION('ref_axis',(0.894934391398442,4.02859800883856E-16,0.446197753347437)) ;
#99104=DIRECTION('',(0.894934391398442,-1.5301685632067E-15,0.446197753347436)) ;
#99105=DIRECTION('',(0.894934391398443,-1.69650395944433E-15,0.446197753347436)) ;
#99106=DIRECTION('center_axis',(0.,-1.,-3.49148133884313E-15)) ;
#99107=DIRECTION('ref_axis',(1.,0.,0.)) ;
#99108=DIRECTION('center_axis',(7.8026127217831E-17,1.,3.64563846986212E-15)) ;
#99109=DIRECTION('ref_axis',(-3.38151074872755E-48,-3.64563846986212E-15,
1.)) ;
#99110=DIRECTION('center_axis',(-1.,0.,0.)) ;
#99111=DIRECTION('ref_axis',(0.,0.,1.)) ;
#99112=DIRECTION('center_axis',(1.,0.,0.)) ;
#99113=DIRECTION('ref_axis',(0.,0.,-1.)) ;
#99114=DIRECTION('center_axis',(-1.,0.,0.)) ;
#99115=DIRECTION('ref_axis',(0.,0.,1.)) ;
#99116=DIRECTION('center_axis',(-1.,0.,0.)) ;
#99117=DIRECTION('ref_axis',(0.,0.,1.)) ;
#99118=DIRECTION('center_axis',(-1.,0.,0.)) ;
#99119=DIRECTION('ref_axis',(0.,0.,1.)) ;
#99120=DIRECTION('center_axis',(-1.,0.,0.)) ;
#99121=DIRECTION('ref_axis',(0.,0.,1.)) ;
#99122=DIRECTION('center_axis',(-1.,0.,0.)) ;
#99123=DIRECTION('ref_axis',(0.,3.67517835871524E-15,-1.)) ;
#99124=DIRECTION('center_axis',(-1.,0.,0.)) ;
#99125=DIRECTION('ref_axis',(0.,0.,1.)) ;
#99126=DIRECTION('center_axis',(-1.,0.,0.)) ;
#99127=DIRECTION('ref_axis',(0.,0.,1.)) ;
#99128=DIRECTION('center_axis',(-1.,0.,0.)) ;
#99129=DIRECTION('ref_axis',(0.,0.,1.)) ;
#126367=CARTESIAN_POINT('',(0.,0.,0.)) ;
#126368=CARTESIAN_POINT('Origin',(-998.069344648895,0.,0.)) ;
#126369=CARTESIAN_POINT('',(1.93065535110549,-2.07039899118859E-17,0.)) ;
#126370=CARTESIAN_POINT('',(1.75000000000779,-6.80903620330553E-17,-0.55600000000311)) ;
#126371=CARTESIAN_POINT('',(-998.069344648895,-3.76907529259025E-13,-3077.68353717531)) ;
#126372=CARTESIAN_POINT('',(1.75,-0.175779377683682,-0.527482331818932)) ;
#126373=CARTESIAN_POINT('Origin',(1.75,0.,0.)) ;
#126374=CARTESIAN_POINT('',(1.75,-0.369999999999998,-0.415013252800438)) ;
#126375=CARTESIAN_POINT('Origin',(1.75,0.,0.)) ;
#126376=CARTESIAN_POINT('',(1.75,-0.415013252800437,-0.370000000000001)) ;
#126377=CARTESIAN_POINT('Origin',(1.75,0.,0.)) ;
#126378=CARTESIAN_POINT('',(1.75,-0.527482331818932,-0.175779377683682)) ;
#126379=CARTESIAN_POINT('Origin',(1.75,0.,0.)) ;
#126380=CARTESIAN_POINT('',(1.75,-0.527482331818932,0.175779377683681)) ;
#126381=CARTESIAN_POINT('Origin',(1.75,0.,0.)) ;
#126382=CARTESIAN_POINT('',(1.75,-0.415013252800437,0.37)) ;
#126383=CARTESIAN_POINT('Origin',(1.75,0.,0.)) ;
#126384=CARTESIAN_POINT('',(1.75,-0.370000000000001,0.415013252800437)) ;
#126385=CARTESIAN_POINT('Origin',(1.75,0.,0.)) ;
#126386=CARTESIAN_POINT('',(1.75,-0.175779377683684,0.527482331818931)) ;
#126387=CARTESIAN_POINT('Origin',(1.75,0.,0.)) ;
#126388=CARTESIAN_POINT('',(1.75,0.175779377683681,0.527482331818932)) ;
#126389=CARTESIAN_POINT('Origin',(1.75,0.,0.)) ;
#126390=CARTESIAN_POINT('',(1.75,0.369999999999999,0.415013252800439)) ;
#126391=CARTESIAN_POINT('Origin',(1.75,0.,0.)) ;
#126392=CARTESIAN_POINT('',(1.75,0.415013252800437,0.37)) ;
#126393=CARTESIAN_POINT('Origin',(1.75,0.,0.)) ;
#126394=CARTESIAN_POINT('',(1.75,0.527482331818932,0.175779377683681)) ;
#126395=CARTESIAN_POINT('Origin',(1.75,0.,0.)) ;
#126396=CARTESIAN_POINT('',(1.75,0.527482331818932,-0.175779377683681)) ;
#126397=CARTESIAN_POINT('Origin',(1.75,0.,0.)) ;
#126398=CARTESIAN_POINT('',(1.75,0.415013252800437,-0.370000000000001)) ;
#126399=CARTESIAN_POINT('Origin',(1.75,0.,0.)) ;
#126400=CARTESIAN_POINT('',(1.75,0.370000000000001,-0.415013252800437)) ;
#126401=CARTESIAN_POINT('Origin',(1.75,0.,0.)) ;
#126402=CARTESIAN_POINT('',(1.75,0.175779377683685,-0.527482331818931)) ;
#126403=CARTESIAN_POINT('Origin',(1.75,0.,0.)) ;
#126404=CARTESIAN_POINT('Origin',(1.75,0.,0.)) ;
#126405=CARTESIAN_POINT('Origin',(1.75,0.,0.)) ;
#126406=CARTESIAN_POINT('Origin',(2.66965268827524,7.90481402181727E-13,
0.0689604923272864)) ;
#126407=CARTESIAN_POINT('Origin',(2.5,0.,0.)) ;
#126408=CARTESIAN_POINT('',(2.4,-1.95943487863577E-16,-1.6)) ;
#126409=CARTESIAN_POINT('Origin',(2.4,0.,0.)) ;
#126410=CARTESIAN_POINT('',(2.5,-1.83697019872103E-16,-1.5)) ;
#126411=CARTESIAN_POINT('Origin',(2.5,-1.95943487863577E-16,-1.6)) ;
#126412=CARTESIAN_POINT('Origin',(2.5,0.,0.)) ;
#126413=CARTESIAN_POINT('Origin',(1.00350153259131,0.,0.)) ;
#126414=CARTESIAN_POINT('',(0.775371598933733,-3.27521818376618E-16,-2.67441860465116)) ;
#126415=CARTESIAN_POINT('Origin',(0.775371598933733,0.,0.)) ;
#126416=CARTESIAN_POINT('',(1.00350153259131,-3.42901103761259E-16,-2.8)) ;
#126417=CARTESIAN_POINT('Origin',(1.00350153259131,-3.0983564018428E-16,
-2.53)) ;
#126418=CARTESIAN_POINT('Origin',(1.00350153259131,0.,0.)) ;
#126419=CARTESIAN_POINT('Origin',(-25.4,0.,0.)) ;
#126420=CARTESIAN_POINT('',(2.4,-3.42901103761259E-16,-2.8)) ;
#126421=CARTESIAN_POINT('',(-25.4,-3.42901103761259E-16,-2.8)) ;
#126422=CARTESIAN_POINT('Origin',(2.4,0.,0.)) ;
#126423=CARTESIAN_POINT('Origin',(-25.4,0.,0.)) ;
#126424=CARTESIAN_POINT('',(6.40000000000001,-1.83697019872103E-16,-1.5)) ;
#126425=CARTESIAN_POINT('',(-25.4,-1.83697019872103E-16,-1.5)) ;
#126426=CARTESIAN_POINT('Origin',(6.4,0.,0.)) ;
#126427=CARTESIAN_POINT('Origin',(5.,-7.47034547479885E-16,0.)) ;
#126428=CARTESIAN_POINT('',(0.18786973422864,1.30633162146802,-0.37)) ;
#126429=CARTESIAN_POINT('',(0.18786973422864,1.30633162146802,0.37)) ;
#126430=CARTESIAN_POINT('Origin',(4.56358262530798,-0.875317983305919,0.)) ;
#126431=CARTESIAN_POINT('',(0.0457951200896417,0.56476013304091,0.37)) ;
#126432=CARTESIAN_POINT('Origin',(5.,-8.04072685956911E-16,0.37)) ;
#126433=CARTESIAN_POINT('',(0.0457951200896434,0.369999999999998,0.564760133040918)) ;
#126434=CARTESIAN_POINT('Origin',(0.0457951200896417,-7.47034547479885E-16,
0.)) ;
#126435=CARTESIAN_POINT('',(0.187869734228641,0.369999999999995,1.30633162146802)) ;
#126436=CARTESIAN_POINT('Origin',(5.,0.37,1.29184809537196E-15)) ;
#126437=CARTESIAN_POINT('',(0.187869734228641,-0.370000000000004,1.30633162146802)) ;
#126438=CARTESIAN_POINT('Origin',(4.56358262530798,2.30912185678654E-15,
-0.875317983305919)) ;
#126439=CARTESIAN_POINT('',(0.045795120089643,-0.370000000000002,0.564760133040916)) ;
#126440=CARTESIAN_POINT('Origin',(5.,-0.37,-1.34888623384898E-15)) ;
#126441=CARTESIAN_POINT('',(0.0457951200896417,-0.564760133040912,0.37)) ;
#126442=CARTESIAN_POINT('Origin',(0.0457951200896417,-7.47034547479885E-16,
0.)) ;
#126443=CARTESIAN_POINT('',(0.18786973422864,-1.30633162146802,0.369999999999999)) ;
#126444=CARTESIAN_POINT('Origin',(5.,-8.04072685956911E-16,0.37)) ;
#126445=CARTESIAN_POINT('',(0.18786973422864,-1.30633162146802,-0.37)) ;
#126446=CARTESIAN_POINT('Origin',(4.56358262530798,0.875317983305919,0.)) ;
#126447=CARTESIAN_POINT('',(0.0457951200896417,-0.564760133040916,-0.37)) ;
#126448=CARTESIAN_POINT('Origin',(5.,-7.47034547479885E-16,-0.37)) ;
#126449=CARTESIAN_POINT('',(0.0457951200896434,-0.369999999999998,-0.564760133040918)) ;
#126450=CARTESIAN_POINT('Origin',(0.0457951200896417,-7.47034547479885E-16,
0.)) ;
#126451=CARTESIAN_POINT('',(0.18786973422864,-0.369999999999995,-1.30633162146802)) ;
#126452=CARTESIAN_POINT('Origin',(5.,-0.37,-1.34888623384898E-15)) ;
#126453=CARTESIAN_POINT('',(0.18786973422864,0.370000000000004,-1.30633162146802)) ;
#126454=CARTESIAN_POINT('Origin',(4.56358262530798,-3.80319095174631E-15,
0.875317983305919)) ;
#126455=CARTESIAN_POINT('',(0.0457951200896425,0.370000000000002,-0.564760133040916)) ;
#126456=CARTESIAN_POINT('Origin',(5.,0.37,1.29184809537196E-15)) ;
#126457=CARTESIAN_POINT('',(0.0457951200896417,0.564760133040915,-0.37)) ;
#126458=CARTESIAN_POINT('Origin',(0.0457951200896417,-7.47034547479885E-16,
0.)) ;
#126459=CARTESIAN_POINT('Origin',(5.,-7.47034547479885E-16,-0.37)) ;
#126460=CARTESIAN_POINT('Origin',(1.75,0.527482331818931,-0.37)) ;
#126461=CARTESIAN_POINT('Ctrl Pts',(0.0457951200892473,0.564760133040949,
-0.37)) ;
#126462=CARTESIAN_POINT('Ctrl Pts',(1.02813143236002,0.48263940638371,-0.37)) ;
#126463=CARTESIAN_POINT('Ctrl Pts',(1.75000000000145,0.415013252800303,
-0.37)) ;
#126464=CARTESIAN_POINT('',(1.75,0.527482331818932,-0.37)) ;
#126465=CARTESIAN_POINT('',(1.75,-0.527482331818931,-0.37)) ;
#126466=CARTESIAN_POINT('',(0.,1.4,-0.37)) ;
#126467=CARTESIAN_POINT('Origin',(1.75,0.527482331818931,-0.37)) ;
#126468=CARTESIAN_POINT('',(1.75,-0.527482331818931,-0.37)) ;
#126469=CARTESIAN_POINT('',(1.75,-0.527482331818931,-0.37)) ;
#126470=CARTESIAN_POINT('Ctrl Pts',(1.75000000000145,-0.415013252800302,
-0.37)) ;
#126471=CARTESIAN_POINT('Ctrl Pts',(1.02813143236002,-0.48263940638371,
-0.37)) ;
#126472=CARTESIAN_POINT('Ctrl Pts',(0.0457951200892475,-0.564760133040949,
-0.37)) ;
#126473=CARTESIAN_POINT('',(0.,-1.4,-0.37)) ;
#126474=CARTESIAN_POINT('Origin',(1.75,-0.527482331818931,0.37)) ;
#126475=CARTESIAN_POINT('',(1.75,0.527482331818932,0.37)) ;
#126476=CARTESIAN_POINT('',(1.75,0.527482331818931,0.37)) ;
#126477=CARTESIAN_POINT('Ctrl Pts',(1.75000000000145,0.415013252800303,
0.37)) ;
#126478=CARTESIAN_POINT('Ctrl Pts',(1.02813143236001,0.482639406383711,
0.37)) ;
#126479=CARTESIAN_POINT('Ctrl Pts',(0.0457951200892475,0.564760133040949,
0.37)) ;
#126480=CARTESIAN_POINT('',(0.,1.4,0.37)) ;
#126481=CARTESIAN_POINT('Origin',(1.75,-0.527482331818931,0.37)) ;
#126482=CARTESIAN_POINT('Ctrl Pts',(0.0457951200892472,-0.56476013304095,
0.37)) ;
#126483=CARTESIAN_POINT('Ctrl Pts',(1.02813143236001,-0.482639406383711,
0.37)) ;
#126484=CARTESIAN_POINT('Ctrl Pts',(1.75000000000145,-0.415013252800303,
0.37)) ;
#126485=CARTESIAN_POINT('',(1.75,-0.527482331818931,0.37)) ;
#126486=CARTESIAN_POINT('',(1.75,0.527482331818931,0.37)) ;
#126487=CARTESIAN_POINT('',(0.,-1.4,0.369999999999999)) ;
#126488=CARTESIAN_POINT('Origin',(1.75,0.527482331818931,0.37)) ;
#126489=CARTESIAN_POINT('Origin',(2.6696526882827,0.0689604923235791,0.)) ;
#126490=CARTESIAN_POINT('',(1.75,0.527482331818931,0.37)) ;
#126491=CARTESIAN_POINT('',(1.75,0.527482331818931,0.37)) ;
#126492=CARTESIAN_POINT('Origin',(0.,-1.4,-0.37)) ;
#126493=CARTESIAN_POINT('Origin',(2.66965268828244,-0.0689604923237097,
2.08166817117217E-16)) ;
#126494=CARTESIAN_POINT('',(1.75,-0.527482331818931,-0.37)) ;
#126495=CARTESIAN_POINT('',(1.75,-0.527482331818931,-0.37)) ;
#126496=CARTESIAN_POINT('Origin',(1.75,0.527482331818931,-0.37)) ;
#126497=CARTESIAN_POINT('',(1.75,-0.370000000000002,0.52748233181893)) ;
#126498=CARTESIAN_POINT('',(1.75,-0.370000000000002,0.52748233181893)) ;
#126499=CARTESIAN_POINT('',(1.75,-0.370000000000002,0.52748233181893)) ;
#126500=CARTESIAN_POINT('Origin',(1.75,0.527482331818931,-0.37)) ;
#126501=CARTESIAN_POINT('Origin',(1.75,0.527482331818931,-0.37)) ;
#126502=CARTESIAN_POINT('Origin',(1.75,0.527482331818931,-0.37)) ;
#126503=CARTESIAN_POINT('',(1.75,-0.369999999999998,-0.527482331818932)) ;
#126504=CARTESIAN_POINT('',(1.75,-0.370000000000002,0.52748233181893)) ;
#126505=CARTESIAN_POINT('',(1.75,0.370000000000002,-0.52748233181893)) ;
#126506=CARTESIAN_POINT('Origin',(1.75,0.527482331818931,-0.37)) ;
#126507=CARTESIAN_POINT('',(1.75,0.370000000000002,-0.52748233181893)) ;
#126508=CARTESIAN_POINT('',(1.75,0.370000000000002,-0.52748233181893)) ;
#126509=CARTESIAN_POINT('',(1.75,0.370000000000002,-0.52748233181893)) ;
#126510=CARTESIAN_POINT('Origin',(1.75,0.527482331818931,-0.37)) ;
#126511=CARTESIAN_POINT('Origin',(1.75,0.527482331818931,-0.37)) ;
#126512=CARTESIAN_POINT('Origin',(1.75,0.369999999999998,0.527482331818933)) ;
#126513=CARTESIAN_POINT('Ctrl Pts',(0.0457951200892495,0.369999999999998,
0.564760133040951)) ;
#126514=CARTESIAN_POINT('Ctrl Pts',(1.02813143235992,0.369999999999998,
0.48263940638372)) ;
#126515=CARTESIAN_POINT('Ctrl Pts',(1.75000000000145,0.369999999999999,
0.415013252800303)) ;
#126516=CARTESIAN_POINT('',(1.75,0.369999999999998,0.527482331818933)) ;
#126517=CARTESIAN_POINT('',(1.75,0.370000000000002,-0.52748233181893)) ;
#126518=CARTESIAN_POINT('',(0.,0.369999999999995,1.4)) ;
#126519=CARTESIAN_POINT('Origin',(1.75,-0.369999999999998,-0.527482331818932)) ;
#126520=CARTESIAN_POINT('Ctrl Pts',(1.75000000000145,-0.370000000000001,
0.4150132528003)) ;
#126521=CARTESIAN_POINT('Ctrl Pts',(1.02813143235991,-0.370000000000002,
0.482639406383718)) ;
#126522=CARTESIAN_POINT('Ctrl Pts',(0.0457951200892481,-0.370000000000002,
0.564760133040949)) ;
#126523=CARTESIAN_POINT('',(0.,-0.370000000000005,1.4)) ;
#126524=CARTESIAN_POINT('Origin',(1.75,-0.370000000000002,0.52748233181893)) ;
#126525=CARTESIAN_POINT('',(1.75,-0.370000000000002,0.52748233181893)) ;
#126526=CARTESIAN_POINT('Origin',(0.,0.370000000000005,-1.4)) ;
#126527=CARTESIAN_POINT('Origin',(2.6696526882837,2.04697370165263E-15,
-0.0689604923230734)) ;
#126528=CARTESIAN_POINT('',(0.,0.370000000000005,-1.4)) ;
#126529=CARTESIAN_POINT('',(0.,-0.369999999999995,-1.4)) ;
#126530=CARTESIAN_POINT('Origin',(1.75,0.369999999999998,0.527482331818933)) ;
#126531=CARTESIAN_POINT('Ctrl Pts',(1.75000000000145,0.370000000000001,
-0.415013252800299)) ;
#126532=CARTESIAN_POINT('Ctrl Pts',(1.02813143235982,0.370000000000002,
-0.482639406383727)) ;
#126533=CARTESIAN_POINT('Ctrl Pts',(0.0457951200892477,0.370000000000002,
-0.56476013304095)) ;
#126534=CARTESIAN_POINT('Origin',(1.75,-0.369999999999998,-0.527482331818932)) ;
#126535=CARTESIAN_POINT('Ctrl Pts',(0.0457951200892493,-0.369999999999998,
-0.564760133040952)) ;
#126536=CARTESIAN_POINT('Ctrl Pts',(1.0281314323599,-0.369999999999998,
-0.482639406383722)) ;
#126537=CARTESIAN_POINT('Ctrl Pts',(1.75000000000145,-0.369999999999998,
-0.415013252800303)) ;
#126538=CARTESIAN_POINT('Origin',(2.4,1.5,0.)) ;
#126539=CARTESIAN_POINT('Origin',(6.4,1.5,0.)) ;
#126540=CARTESIAN_POINT('Origin',(1.75,0.527482331818931,-0.37)) ;
#126541=CARTESIAN_POINT('Origin',(1.75,0.,0.)) ;
#126542=CARTESIAN_POINT('Origin',(1.75,0.,0.)) ;
#126543=CARTESIAN_POINT('Origin',(1.75,0.,0.)) ;
#126544=CARTESIAN_POINT('Origin',(1.75,0.,0.)) ;
#126545=CARTESIAN_POINT('Origin',(1.75,0.,0.)) ;
#126546=CARTESIAN_POINT('Origin',(1.75,0.,0.)) ;
#126547=CARTESIAN_POINT('Origin',(1.75,0.,0.)) ;
#126562=UNCERTAINTY_MEASURE_WITH_UNIT(LENGTH_MEASURE(0.01),#126572,
'DISTANCE_ACCURACY_VALUE',
'Maximum model space distance between geometric entities at asserted c
onnectivities') ;
#126563=UNCERTAINTY_MEASURE_WITH_UNIT(LENGTH_MEASURE(0.01),#126572,
'DISTANCE_ACCURACY_VALUE',
'Maximum model space distance between geometric entities at asserted c
onnectivities') ;
#126570=(
GEOMETRIC_REPRESENTATION_CONTEXT(3)
GLOBAL_UNCERTAINTY_ASSIGNED_CONTEXT((#126562))
GLOBAL_UNIT_ASSIGNED_CONTEXT((#126572,#126574,#126575))
REPRESENTATION_CONTEXT('','3D')
) ;
#126571=(
GEOMETRIC_REPRESENTATION_CONTEXT(3)
GLOBAL_UNCERTAINTY_ASSIGNED_CONTEXT((#126563))
GLOBAL_UNIT_ASSIGNED_CONTEXT((#126572,#126574,#126575))
REPRESENTATION_CONTEXT('','3D')
) ;
#126572=(
LENGTH_UNIT()
NAMED_UNIT(*)
SI_UNIT(.MILLI.,.METRE.)
) ;
#126574=(
NAMED_UNIT(*)
PLANE_ANGLE_UNIT()
SI_UNIT($,.RADIAN.)
) ;
#126575=(
NAMED_UNIT(*)
SI_UNIT($,.STERADIAN.)
SOLID_ANGLE_UNIT()
) ;
#126582=SHAPE_DEFINITION_REPRESENTATION(#126589,#126604) ;
#126589=PRODUCT_DEFINITION_SHAPE('',$,#126612) ;
#126604=SHAPE_REPRESENTATION('',(#76762),#126570) ;
#126605=PRODUCT_DEFINITION_CONTEXT('part definition',#126628,'design') ;
#126612=PRODUCT_DEFINITION('Screw_ISO7045_M3x4','Screw_ISO7045_M3x4',#126619,
#126605) ;
#126619=PRODUCT_DEFINITION_FORMATION('',$,#126636) ;
#126628=APPLICATION_CONTEXT(
'Core Data for Automotive Mechanical Design Process') ;
#126629=PRODUCT_CONTEXT('part definition',#126628,'mechanical') ;
#126636=PRODUCT('Screw_ISO7045_M3x4','Screw_ISO7045_M3x4',$,(#126629)) ;
#126645=PRESENTATION_STYLE_ASSIGNMENT((#126654)) ;
#126654=SURFACE_STYLE_USAGE(.BOTH.,#126663) ;
#126663=SURFACE_SIDE_STYLE('',(#126672)) ;
#126672=SURFACE_STYLE_FILL_AREA(#126681) ;
#126681=FILL_AREA_STYLE('Opaque(198,193,188)',(#126690)) ;
#126690=FILL_AREA_STYLE_COLOUR('Opaque(198,193,188)',#126699) ;
#126699=COLOUR_RGB('Opaque(198,193,188)', 0.40784314, 0.44705882, 0.49803922) ;
ENDSEC;
END-ISO-10303-21;
